ISO-10303-21;
HEADER;
/* Generated by software containing ST-Developer
 * from STEP Tools, Inc. (www.steptools.com) 
 */

FILE_DESCRIPTION(
/* description */ ('Over-Centre Plunger Toggle Clamp on Slotted Fixture Frame'),
/* implementation_level */ '2;1');

FILE_NAME(
/* name */ 
'Link bush (1).step',
/* time_stamp */ '2026-10-28T03:23:24-07:00',
/* author */ (''),
/* organization */ (''),
/* preprocessor_version */ 'ST-DEVELOPER v20.2',
/* originating_system */ 'Autodesk Translation Framework v15.17.0.0',
/* authorisation */ '');

FILE_SCHEMA (('AUTOMOTIVE_DESIGN { 1 0 10303 214 3 1 1 }'));
ENDSEC;

DATA;
#10=MECHANICAL_DESIGN_GEOMETRIC_PRESENTATION_REPRESENTATION('',(#558),#15212);
#466=SHAPE_REPRESENTATION_RELATIONSHIP('SRR','None',#15444,#508);
#508=ADVANCED_BREP_SHAPE_REPRESENTATION('',(#605),#15206);
#558=STYLED_ITEM('',(#15733),#605);
#605=MANIFOLD_SOLID_BREP('Body1',#8294);
#774=FACE_BOUND('',#2177,.T.);
#775=FACE_BOUND('',#2179,.T.);
#1052=PLANE('',#9667);
#1053=PLANE('',#9668);
#1525=FACE_OUTER_BOUND('',#2174,.T.);
#1526=FACE_OUTER_BOUND('',#2175,.T.);
#1527=FACE_OUTER_BOUND('',#2176,.T.);
#1528=FACE_OUTER_BOUND('',#2178,.T.);
#2174=EDGE_LOOP('',(#7425,#7426,#7427,#7428));
#2175=EDGE_LOOP('',(#7429,#7430,#7431,#7432));
#2176=EDGE_LOOP('',(#7433));
#2177=EDGE_LOOP('',(#7434));
#2178=EDGE_LOOP('',(#7435));
#2179=EDGE_LOOP('',(#7436));
#2796=LINE('',#14876,#3426);
#2797=LINE('',#14882,#3427);
#3426=VECTOR('',#12119,0.305);
#3427=VECTOR('',#12126,0.5);
#3830=CIRCLE('',#9662,0.305);
#3831=CIRCLE('',#9663,0.305);
#3832=CIRCLE('',#9665,0.5);
#3833=CIRCLE('',#9666,0.5);
#4482=VERTEX_POINT('',#14873);
#4483=VERTEX_POINT('',#14875);
#4484=VERTEX_POINT('',#14879);
#4485=VERTEX_POINT('',#14881);
#5473=EDGE_CURVE('',#4482,#4482,#3830,.T.);
#5474=EDGE_CURVE('',#4482,#4483,#2796,.T.);
#5475=EDGE_CURVE('',#4483,#4483,#3831,.T.);
#5476=EDGE_CURVE('',#4484,#4484,#3832,.T.);
#5477=EDGE_CURVE('',#4484,#4485,#2797,.T.);
#5478=EDGE_CURVE('',#4485,#4485,#3833,.T.);
#7425=ORIENTED_EDGE('',*,*,#5473,.F.);
#7426=ORIENTED_EDGE('',*,*,#5474,.T.);
#7427=ORIENTED_EDGE('',*,*,#5475,.T.);
#7428=ORIENTED_EDGE('',*,*,#5474,.F.);
#7429=ORIENTED_EDGE('',*,*,#5476,.F.);
#7430=ORIENTED_EDGE('',*,*,#5477,.T.);
#7431=ORIENTED_EDGE('',*,*,#5478,.T.);
#7432=ORIENTED_EDGE('',*,*,#5477,.F.);
#7433=ORIENTED_EDGE('',*,*,#5476,.T.);
#7434=ORIENTED_EDGE('',*,*,#5473,.T.);
#7435=ORIENTED_EDGE('',*,*,#5478,.F.);
#7436=ORIENTED_EDGE('',*,*,#5475,.F.);
#7748=CYLINDRICAL_SURFACE('',#9661,0.305);
#7749=CYLINDRICAL_SURFACE('',#9664,0.5);
#8197=ADVANCED_FACE('',(#1525),#7748,.F.);
#8198=ADVANCED_FACE('',(#1526),#7749,.T.);
#8199=ADVANCED_FACE('',(#1527,#774),#1052,.T.);
#8200=ADVANCED_FACE('',(#1528,#775),#1053,.F.);
#8294=CLOSED_SHELL('',(#8197,#8198,#8199,#8200));
#9660=AXIS2_PLACEMENT_3D('',#14871,#12113,#12114);
#9661=AXIS2_PLACEMENT_3D('',#14872,#12115,#12116);
#9662=AXIS2_PLACEMENT_3D('',#14874,#12117,#12118);
#9663=AXIS2_PLACEMENT_3D('',#14877,#12120,#12121);
#9664=AXIS2_PLACEMENT_3D('',#14878,#12122,#12123);
#9665=AXIS2_PLACEMENT_3D('',#14880,#12124,#12125);
#9666=AXIS2_PLACEMENT_3D('',#14883,#12127,#12128);
#9667=AXIS2_PLACEMENT_3D('',#14884,#12129,#12130);
#9668=AXIS2_PLACEMENT_3D('',#14885,#12131,#12132);
#12113=DIRECTION('axis',(0.,0.,1.));
#12114=DIRECTION('refdir',(1.,0.,0.));
#12115=DIRECTION('center_axis',(0.,1.,0.));
#12116=DIRECTION('ref_axis',(1.,0.,0.));
#12117=DIRECTION('center_axis',(0.,-1.,0.));
#12118=DIRECTION('ref_axis',(1.,0.,0.));
#12119=DIRECTION('',(0.,-1.,0.));
#12120=DIRECTION('center_axis',(0.,-1.,0.));
#12121=DIRECTION('ref_axis',(1.,0.,0.));
#12122=DIRECTION('center_axis',(0.,1.,0.));
#12123=DIRECTION('ref_axis',(1.,0.,0.));
#12124=DIRECTION('center_axis',(0.,1.,0.));
#12125=DIRECTION('ref_axis',(1.,0.,0.));
#12126=DIRECTION('',(0.,-1.,0.));
#12127=DIRECTION('center_axis',(0.,1.,0.));
#12128=DIRECTION('ref_axis',(1.,0.,0.));
#12129=DIRECTION('center_axis',(0.,1.,0.));
#12130=DIRECTION('ref_axis',(1.,0.,0.));
#12131=DIRECTION('center_axis',(0.,1.,0.));
#12132=DIRECTION('ref_axis',(1.,0.,0.));
#14871=CARTESIAN_POINT('',(0.,0.,0.));
#14872=CARTESIAN_POINT('Origin',(0.,-5.5,4.668081457105));
#14873=CARTESIAN_POINT('',(-0.305,-4.7,4.668081457105));
#14874=CARTESIAN_POINT('Origin',(0.,-4.7,4.668081457105));
#14875=CARTESIAN_POINT('',(-0.305,-5.5,4.668081457105));
#14876=CARTESIAN_POINT('',(-0.305,-5.5,4.668081457105));
#14877=CARTESIAN_POINT('Origin',(0.,-5.5,4.668081457105));
#14878=CARTESIAN_POINT('Origin',(0.,-5.5,4.668081457105));
#14879=CARTESIAN_POINT('',(-0.5,-4.7,4.668081457105));
#14880=CARTESIAN_POINT('Origin',(0.,-4.7,4.668081457105));
#14881=CARTESIAN_POINT('',(-0.5,-5.5,4.668081457105));
#14882=CARTESIAN_POINT('',(-0.5,-5.5,4.668081457105));
#14883=CARTESIAN_POINT('Origin',(0.,-5.5,4.668081457105));
#14884=CARTESIAN_POINT('Origin',(0.,-4.7,4.668081457105));
#14885=CARTESIAN_POINT('Origin',(0.,-5.5,4.668081457105));
#15156=UNCERTAINTY_MEASURE_WITH_UNIT(LENGTH_MEASURE(0.001),#15213,
'DISTANCE_ACCURACY_VALUE',
'Maximum model space distance between geometric entities at asserted c
onnectivities');
#15162=UNCERTAINTY_MEASURE_WITH_UNIT(LENGTH_MEASURE(0.001),#15213,
'DISTANCE_ACCURACY_VALUE',
'Maximum model space distance between geometric entities at asserted c
onnectivities');
#15206=(
GEOMETRIC_REPRESENTATION_CONTEXT(3)
GLOBAL_UNCERTAINTY_ASSIGNED_CONTEXT((#15156))
GLOBAL_UNIT_ASSIGNED_CONTEXT((#15213,#15215,#15216))
REPRESENTATION_CONTEXT('','3D')
);
#15212=(
GEOMETRIC_REPRESENTATION_CONTEXT(3)
GLOBAL_UNCERTAINTY_ASSIGNED_CONTEXT((#15162))
GLOBAL_UNIT_ASSIGNED_CONTEXT((#15213,#15215,#15216))
REPRESENTATION_CONTEXT('','3D')
);
#15213=(
LENGTH_UNIT()
NAMED_UNIT(*)
SI_UNIT(.CENTI.,.METRE.)
);
#15215=(
NAMED_UNIT(*)
PLANE_ANGLE_UNIT()
SI_UNIT($,.RADIAN.)
);
#15216=(
NAMED_UNIT(*)
SI_UNIT($,.STERADIAN.)
SOLID_ANGLE_UNIT()
);
#15260=SHAPE_DEFINITION_REPRESENTATION(#15384,#15444);
#15384=PRODUCT_DEFINITION_SHAPE('',$,#15494);
#15444=SHAPE_REPRESENTATION('',(#9660),#15206);
#15450=PRODUCT_DEFINITION_CONTEXT('part definition',#15599,'design');
#15494=PRODUCT_DEFINITION('Link bush (1)','Link bush (1)',#15543,#15450);
#15543=PRODUCT_DEFINITION_FORMATION('',$,#15644);
#15599=APPLICATION_CONTEXT(
'Core Data for Automotive Mechanical Design Process');
#15600=PRODUCT_CONTEXT('part definition',#15599,'mechanical');
#15644=PRODUCT('Link bush (1)','Link bush (1)','Link bush (1)',(#15600));
#15727=COLOUR_RGB('Off White',0.89,0.88,0.83);
#15728=FILL_AREA_STYLE_COLOUR('',#15727);
#15729=FILL_AREA_STYLE('',(#15728));
#15730=SURFACE_STYLE_FILL_AREA(#15729);
#15731=SURFACE_SIDE_STYLE('',(#15730));
#15732=SURFACE_STYLE_USAGE(.BOTH.,#15731);
#15733=PRESENTATION_STYLE_ASSIGNMENT((#15732));
ENDSEC;
END-ISO-10303-21;
